ISO-10303-21;
HEADER;
/* Generated by software containing ST-Developer
 * from STEP Tools, Inc. (www.steptools.com) 
 */

FILE_DESCRIPTION(
/* description */ ('Manual piston pump'),
/* implementation_level */ '2;1');

FILE_NAME(
/* name */ 'Short retaining screw.step',
/* time_stamp */ '2026-11-02T16:54:23-08:00',
/* author */ (''),
/* organization */ (''),
/* preprocessor_version */ 'ST-DEVELOPER v20.2',
/* originating_system */ 'Autodesk Translation Framework v15.17.0.0',
/* authorisation */ '');

FILE_SCHEMA (('AUTOMOTIVE_DESIGN { 1 0 10303 214 3 1 1 }'));
ENDSEC;

DATA;
#10=MECHANICAL_DESIGN_GEOMETRIC_PRESENTATION_REPRESENTATION('',(#735),#19043);
#601=SHAPE_REPRESENTATION_RELATIONSHIP('SRR','None',#19349,#664);
#664=ADVANCED_BREP_SHAPE_REPRESENTATION('',(#804),#19016);
#735=STYLED_ITEM('',(#19663),#804);
#804=MANIFOLD_SOLID_BREP('Body1',#9522);
#998=FACE_BOUND('',#2441,.T.);
#1234=CYLINDRICAL_SURFACE('',#11059,0.35);
#1235=CYLINDRICAL_SURFACE('',#11062,0.199999999999999);
#1694=FACE_OUTER_BOUND('',#2440,.T.);
#1695=FACE_OUTER_BOUND('',#2442,.T.);
#1696=FACE_OUTER_BOUND('',#2443,.T.);
#1697=FACE_OUTER_BOUND('',#2444,.T.);
#1698=FACE_OUTER_BOUND('',#2445,.T.);
#2440=EDGE_LOOP('',(#7919));
#2441=EDGE_LOOP('',(#7920));
#2442=EDGE_LOOP('',(#7921,#7922,#7923,#7924));
#2443=EDGE_LOOP('',(#7925));
#2444=EDGE_LOOP('',(#7926,#7927,#7928,#7929));
#2445=EDGE_LOOP('',(#7930));
#3018=CIRCLE('',#11057,0.35);
#3019=CIRCLE('',#11058,0.199999999999999);
#3020=CIRCLE('',#11060,0.35);
#3021=CIRCLE('',#11063,0.199999999999999);
#3569=LINE('',#17930,#4173);
#3570=LINE('',#17936,#4174);
#4173=VECTOR('',#13551,0.35);
#4174=VECTOR('',#13560,0.199999999999999);
#4909=VERTEX_POINT('',#17924);
#4910=VERTEX_POINT('',#17926);
#4911=VERTEX_POINT('',#17929);
#4912=VERTEX_POINT('',#17934);
#5946=EDGE_CURVE('',#4909,#4909,#3018,.T.);
#5947=EDGE_CURVE('',#4910,#4910,#3019,.T.);
#5948=EDGE_CURVE('',#4909,#4911,#3569,.T.);
#5949=EDGE_CURVE('',#4911,#4911,#3020,.T.);
#5950=EDGE_CURVE('',#4912,#4912,#3021,.T.);
#5951=EDGE_CURVE('',#4912,#4910,#3570,.T.);
#7919=ORIENTED_EDGE('',*,*,#5946,.T.);
#7920=ORIENTED_EDGE('',*,*,#5947,.F.);
#7921=ORIENTED_EDGE('',*,*,#5946,.F.);
#7922=ORIENTED_EDGE('',*,*,#5948,.T.);
#7923=ORIENTED_EDGE('',*,*,#5949,.T.);
#7924=ORIENTED_EDGE('',*,*,#5948,.F.);
#7925=ORIENTED_EDGE('',*,*,#5949,.F.);
#7926=ORIENTED_EDGE('',*,*,#5950,.F.);
#7927=ORIENTED_EDGE('',*,*,#5951,.T.);
#7928=ORIENTED_EDGE('',*,*,#5947,.T.);
#7929=ORIENTED_EDGE('',*,*,#5951,.F.);
#7930=ORIENTED_EDGE('',*,*,#5950,.T.);
#8792=PLANE('',#11056);
#8793=PLANE('',#11061);
#8794=PLANE('',#11064);
#9299=ADVANCED_FACE('',(#1694,#998),#8792,.T.);
#9300=ADVANCED_FACE('',(#1695),#1234,.T.);
#9301=ADVANCED_FACE('',(#1696),#8793,.F.);
#9302=ADVANCED_FACE('',(#1697),#1235,.T.);
#9303=ADVANCED_FACE('',(#1698),#8794,.T.);
#9522=CLOSED_SHELL('',(#9299,#9300,#9301,#9302,#9303));
#11055=AXIS2_PLACEMENT_3D('',#17922,#13541,#13542);
#11056=AXIS2_PLACEMENT_3D('',#17923,#13543,#13544);
#11057=AXIS2_PLACEMENT_3D('',#17925,#13545,#13546);
#11058=AXIS2_PLACEMENT_3D('',#17927,#13547,#13548);
#11059=AXIS2_PLACEMENT_3D('',#17928,#13549,#13550);
#11060=AXIS2_PLACEMENT_3D('',#17931,#13552,#13553);
#11061=AXIS2_PLACEMENT_3D('',#17932,#13554,#13555);
#11062=AXIS2_PLACEMENT_3D('',#17933,#13556,#13557);
#11063=AXIS2_PLACEMENT_3D('',#17935,#13558,#13559);
#11064=AXIS2_PLACEMENT_3D('',#17937,#13561,#13562);
#13541=DIRECTION('axis',(0.,0.,1.));
#13542=DIRECTION('refdir',(1.,0.,0.));
#13543=DIRECTION('center_axis',(1.,0.,0.));
#13544=DIRECTION('ref_axis',(0.,0.,-1.));
#13545=DIRECTION('center_axis',(1.,0.,0.));
#13546=DIRECTION('ref_axis',(0.,0.,-1.));
#13547=DIRECTION('center_axis',(1.,0.,0.));
#13548=DIRECTION('ref_axis',(0.,0.,-1.));
#13549=DIRECTION('center_axis',(1.,0.,0.));
#13550=DIRECTION('ref_axis',(0.,0.,-1.));
#13551=DIRECTION('',(-1.,0.,0.));
#13552=DIRECTION('center_axis',(1.,0.,0.));
#13553=DIRECTION('ref_axis',(0.,0.,-1.));
#13554=DIRECTION('center_axis',(1.,0.,0.));
#13555=DIRECTION('ref_axis',(0.,0.,-1.));
#13556=DIRECTION('center_axis',(1.,0.,0.));
#13557=DIRECTION('ref_axis',(0.,0.,-1.));
#13558=DIRECTION('center_axis',(1.,0.,0.));
#13559=DIRECTION('ref_axis',(0.,0.,-1.));
#13560=DIRECTION('',(-1.,0.,0.));
#13561=DIRECTION('center_axis',(1.,0.,0.));
#13562=DIRECTION('ref_axis',(0.,0.,-1.));
#17922=CARTESIAN_POINT('',(0.,0.,0.));
#17923=CARTESIAN_POINT('Origin',(-3.2,-2.69185245480489,11.3081475451951));
#17924=CARTESIAN_POINT('',(-3.2,-2.69185245480489,11.6581475451951));
#17925=CARTESIAN_POINT('Origin',(-3.2,-2.69185245480489,11.3081475451951));
#17926=CARTESIAN_POINT('',(-3.2,-2.69185245480489,11.5081475451951));
#17927=CARTESIAN_POINT('Origin',(-3.2,-2.69185245480489,11.3081475451951));
#17928=CARTESIAN_POINT('Origin',(-3.6,-2.69185245480489,11.3081475451951));
#17929=CARTESIAN_POINT('',(-3.6,-2.69185245480489,11.6581475451951));
#17930=CARTESIAN_POINT('',(-3.6,-2.69185245480489,11.6581475451951));
#17931=CARTESIAN_POINT('Origin',(-3.6,-2.69185245480489,11.3081475451951));
#17932=CARTESIAN_POINT('Origin',(-3.6,-2.69185245480489,11.3081475451951));
#17933=CARTESIAN_POINT('Origin',(-3.2,-2.69185245480489,11.3081475451951));
#17934=CARTESIAN_POINT('',(-2.5,-2.69185245480489,11.5081475451951));
#17935=CARTESIAN_POINT('Origin',(-2.5,-2.69185245480489,11.3081475451951));
#17936=CARTESIAN_POINT('',(-3.2,-2.69185245480489,11.5081475451951));
#17937=CARTESIAN_POINT('Origin',(-2.5,-2.69185245480489,11.3081475451951));
#18945=UNCERTAINTY_MEASURE_WITH_UNIT(LENGTH_MEASURE(0.001),#19044,
'DISTANCE_ACCURACY_VALUE',
'Maximum model space distance between geometric entities at asserted c
onnectivities');
#18972=UNCERTAINTY_MEASURE_WITH_UNIT(LENGTH_MEASURE(0.001),#19044,
'DISTANCE_ACCURACY_VALUE',
'Maximum model space distance between geometric entities at asserted c
onnectivities');
#19016=(
GEOMETRIC_REPRESENTATION_CONTEXT(3)
GLOBAL_UNCERTAINTY_ASSIGNED_CONTEXT((#18945))
GLOBAL_UNIT_ASSIGNED_CONTEXT((#19044,#19046,#19047))
REPRESENTATION_CONTEXT('','3D')
);
#19043=(
GEOMETRIC_REPRESENTATION_CONTEXT(3)
GLOBAL_UNCERTAINTY_ASSIGNED_CONTEXT((#18972))
GLOBAL_UNIT_ASSIGNED_CONTEXT((#19044,#19046,#19047))
REPRESENTATION_CONTEXT('','3D')
);
#19044=(
LENGTH_UNIT()
NAMED_UNIT(*)
SI_UNIT(.CENTI.,.METRE.)
);
#19046=(
NAMED_UNIT(*)
PLANE_ANGLE_UNIT()
SI_UNIT($,.RADIAN.)
);
#19047=(
NAMED_UNIT(*)
SI_UNIT($,.STERADIAN.)
SOLID_ANGLE_UNIT()
);
#19091=SHAPE_DEFINITION_REPRESENTATION(#19168,#19349);
#19168=PRODUCT_DEFINITION_SHAPE('',$,#19420);
#19349=SHAPE_REPRESENTATION('',(#11055),#19016);
#19376=PRODUCT_DEFINITION_CONTEXT('part definition',#19588,'design');
#19420=PRODUCT_DEFINITION('2026-11-03-00-38-46-464',
'Short retaining screw',#19490,#19376);
#19490=PRODUCT_DEFINITION_FORMATION('',$,#19633);
#19588=APPLICATION_CONTEXT(
'Core Data for Automotive Mechanical Design Process');
#19589=PRODUCT_CONTEXT('part definition',#19588,'mechanical');
#19633=PRODUCT('2026-11-03-00-38-46-464','Short retaining screw',
'Short retaining screw',(#19589));
#19663=PRESENTATION_STYLE_ASSIGNMENT((#19669));
#19669=SURFACE_STYLE_USAGE(.BOTH.,#19675);
#19675=SURFACE_SIDE_STYLE('',(#19681));
#19681=SURFACE_STYLE_FILL_AREA(#19687);
#19687=FILL_AREA_STYLE('CAD Library Painted - Graphite',(#19693));
#19693=FILL_AREA_STYLE_COLOUR('CAD Library Painted - Graphite',#19699);
#19699=COLOUR_RGB('CAD Library Painted - Graphite',0.168627450980392,0.192156862745098,
0.231372549019608);
ENDSEC;
END-ISO-10303-21;
